ISO-10303-21;
HEADER;
FILE_DESCRIPTION (('STEP AP203'),
    '1' );
FILE_NAME ('1602p_c_11.step',
    '2026-10-31T14:11:27',
    ( '' ),
    ( '' ),
    'SwSTEP 2.0',
    'SolidWorks 2024',
    '' );
FILE_SCHEMA (( 'AUTOMOTIVE_DESIGN' ));
ENDSEC;

DATA;
#73=CIRCLE ( 'NONE', #5027, 49.22658835543908395 ) ;
#205=DIRECTION ( 'NONE',  ( 0.02168293104353429326, -0.9997648976141146893, 2.442038521257509372E-15 ) ) ;
#225=ORIENTED_EDGE ( 'NONE', *, *, #9354, .F. ) ;
#235=AXIS2_PLACEMENT_3D ( 'NONE', #21631, #7407, #21868 ) ;
#281=AXIS2_PLACEMENT_3D ( 'NONE', #8014, #22242, #9805 ) ;
#313=EDGE_CURVE ( 'NONE', #8111, #8468, #10967, .T. ) ;
#328=APPLICATION_CONTEXT ( 'configuration controlled 3d designs of mechanical parts and assemblies' ) ;
#375=DIRECTION ( 'NONE',  ( -3.210834492181040124E-17, 2.441916418604790135E-15, 1.000000000000000000 ) ) ;
#404=VERTEX_POINT ( 'NONE', #8293 ) ;
#415=DIRECTION ( 'NONE',  ( 1.000000000000000000, 0.000000000000000000, 0.000000000000000000 ) ) ;
#452=ORIENTED_EDGE ( 'NONE', *, *, #18200, .T. ) ;
#470=DIRECTION ( 'NONE',  ( -0.9997648975362233292, -0.02168293463498000007, 0.000000000000000000 ) ) ;
#473=APPLICATION_CONTEXT ( 'configuration controlled 3d designs of mechanical parts and assemblies' ) ;
#545=EDGE_CURVE ( 'NONE', #3168, #668, #1035, .T. ) ;
#551=VERTEX_POINT ( 'NONE', #15995 ) ;
#604=ORIENTED_EDGE ( 'NONE', *, *, #13332, .T. ) ;
#638=VERTEX_POINT ( 'NONE', #16114 ) ;
#667=FACE_OUTER_BOUND ( 'NONE', #10413, .T. ) ;
#668=VERTEX_POINT ( 'NONE', #7792 ) ;
#693=FACE_OUTER_BOUND ( 'NONE', #12076, .T. ) ;
#699=CARTESIAN_POINT ( 'NONE',  ( -20.00000000397369959, 22.95208919256949898, -3.750000000000059508 ) ) ;
#820=EDGE_LOOP ( 'NONE', ( #21384, #19858, #16833, #7927, #3627, #11636, #14084, #7098, #6887, #15761, #3055 ) ) ;
#843=CARTESIAN_POINT ( 'NONE',  ( -25.49858938551139786, -0.2322002804899490069, -5.000000000000000000 ) ) ;
#860=LINE ( 'NONE', #8129, #5700 ) ;
#891=LINE ( 'NONE', #1118, #14675 ) ;
#922=CYLINDRICAL_SURFACE ( 'NONE', #4671, 5.999999999999999112 ) ;
#932=DIRECTION ( 'NONE',  ( -0.02168293104353429326, 0.9997648976141146893, -2.442038521257509372E-15 ) ) ;
#945=EDGE_CURVE ( 'NONE', #10921, #668, #8380, .T. ) ;
#1035=CIRCLE ( 'NONE', #10560, 2.500000000000000000 ) ;
#1052=EDGE_LOOP ( 'NONE', ( #5105, #5858, #452, #9952 ) ) ;
#1053=DIRECTION ( 'NONE',  ( -0.9997648975362233292, -0.02168293463497958373, 0.000000000000000000 ) ) ;
#1118=CARTESIAN_POINT ( 'NONE',  ( -32.64682763696299617, 7.329162855357659545, -3.750000000000000000 ) ) ;
#1128=LINE ( 'NONE', #19662, #18640 ) ;
#1196=ORIENTED_EDGE ( 'NONE', *, *, #1944, .T. ) ;
#1213=CIRCLE ( 'NONE', #14506, 1.000000000000000888 ) ;
#1278=CARTESIAN_POINT ( 'NONE',  ( -31.64160538070510142, 6.334412527122569969, -5.000000000000000000 ) ) ;
#1290=LINE ( 'NONE', #21016, #1815 ) ;
#1483=EDGE_CURVE ( 'NONE', #21214, #404, #860, .T. ) ;
#1491=DIRECTION ( 'NONE',  ( -0.9997648975362233292, -0.02168293463498000007, 0.000000000000000000 ) ) ;
#1536=CIRCLE ( 'NONE', #14063, 3.499999999999999112 ) ;
#1544=VERTEX_POINT ( 'NONE', #10618 ) ;
#1549=ORIENTED_EDGE ( 'NONE', *, *, #19877, .T. ) ;
#1631=CARTESIAN_POINT ( 'NONE',  ( -21.99941224366415682, -0.1563100308134250105, -2.500000000000000000 ) ) ;
#1663=DIRECTION ( 'NONE',  ( -3.210834492181045054E-17, 2.441916418604795262E-15, 1.000000000000000000 ) ) ;
#1668=ORIENTED_EDGE ( 'NONE', *, *, #8798, .T. ) ;
#1802=FACE_OUTER_BOUND ( 'NONE', #17758, .T. ) ;
#1815=VECTOR ( 'NONE', #932, 1000.000000000000114 ) ;
#1829=LINE ( 'NONE', #21897, #15707 ) ;
#1846=VERTEX_POINT ( 'NONE', #9768 ) ;
#1858=ORIENTED_EDGE ( 'NONE', *, *, #5758, .F. ) ;
#1944=EDGE_CURVE ( 'NONE', #16249, #21214, #7449, .T. ) ;
#2114=DIRECTION ( 'NONE',  ( -0.9997648975362233292, -0.02168293463498000007, 0.000000000000000000 ) ) ;
#2207=CARTESIAN_POINT ( 'NONE',  ( -19.49999999982519938, -0.1021026942257859949, -3.750000000000000000 ) ) ;
#2378=VERTEX_POINT ( 'NONE', #3851 ) ;
#2398=CIRCLE ( 'NONE', #14540, 1.749999999999997780 ) ;
#2399=VERTEX_POINT ( 'NONE', #12774 ) ;
#2484=FACE_OUTER_BOUND ( 'NONE', #19142, .T. ) ;
#2492=AXIS2_PLACEMENT_3D ( 'NONE', #2207, #11625, #7915 ) ;
#2569=CARTESIAN_POINT ( 'NONE',  ( 0.000000000000000000, 0.000000000000000000, 0.000000000000000000 ) ) ;
#2600=CARTESIAN_POINT ( 'NONE',  ( -32.64682763696299617, 7.329162855357659545, -2.500000000000000000 ) ) ;
#2692=DIRECTION ( 'NONE',  ( -3.210834492181045054E-17, 2.441916418604790135E-15, 1.000000000000000000 ) ) ;
#2739=CARTESIAN_POINT ( 'NONE',  ( -30.15704507771850018, 9.287077397714901039, -3.750000000000000000 ) ) ;
#2744=VECTOR ( 'NONE', #9735, 1000.000000000000000 ) ;
#2897=ADVANCED_FACE ( 'NONE', ( #1802 ), #5255, .F. ) ;
#3001=AXIS2_PLACEMENT_3D ( 'NONE', #10521, #10171, #23313 ) ;
#3016=DIRECTION ( 'NONE',  ( -0.9080662505692100872, 0.4188265566761218417, -1.040834085574018826E-15 ) ) ;
#3055=ORIENTED_EDGE ( 'NONE', *, *, #22538, .F. ) ;
#3097=CARTESIAN_POINT ( 'NONE',  ( -20.00000000397369959, 22.95208919256949898, -2.500000000000059952 ) ) ;
#3115=PLANE ( 'NONE',  #11538 ) ;
#3144=CARTESIAN_POINT ( 'NONE',  ( -13.66075527208050033, 1.277470069177119916, -2.500000000000000000 ) ) ;
#3168=VERTEX_POINT ( 'NONE', #1631 ) ;
#3183=DIRECTION ( 'NONE',  ( -0.005235964026270697493, 0.9999862922464064496, -2.442051063555178886E-15 ) ) ;
#3264=( NAMED_UNIT ( * ) PLANE_ANGLE_UNIT ( ) SI_UNIT ( $, .RADIAN. ) );
#3348=DIRECTION ( 'NONE',  ( -1.158391195604533947E-15, 6.607917932627710271E-32, 1.000000000000000000 ) ) ;
#3367=DIRECTION ( 'NONE',  ( 3.210834492180725196E-17, -2.441916418604790135E-15, -1.000000000000000000 ) ) ;
#3380=CARTESIAN_POINT ( 'NONE',  ( -25.44839750738890061, 25.46504853262640111, -2.500000000000059952 ) ) ;
#3389=PLANE ( 'NONE',  #20937 ) ;
#3404=VECTOR ( 'NONE', #4808, 1000.000000000000000 ) ;
#3498=EDGE_CURVE ( 'NONE', #16156, #12721, #19020, .T. ) ;
#3501=( LENGTH_UNIT ( ) NAMED_UNIT ( * ) SI_UNIT ( .MILLI., .METRE. ) );
#3515=CARTESIAN_POINT ( 'NONE',  ( -31.64684134471649912, 7.334398819369050138, -5.000000000000000000 ) ) ;
#3547=ORIENTED_EDGE ( 'NONE', *, *, #13917, .T. ) ;
#3558=ORIENTED_EDGE ( 'NONE', *, *, #3993, .F. ) ;
#3570=ADVANCED_FACE ( 'NONE', ( #667 ), #18971, .F. ) ;
#3627=ORIENTED_EDGE ( 'NONE', *, *, #18200, .F. ) ;
#3644=CYLINDRICAL_SURFACE ( 'NONE', #8177, 1.000000000000000888 ) ;
#3650=CARTESIAN_POINT ( 'NONE',  ( -14.10663218835320087, 21.82654748245090204, -5.000000000000060396 ) ) ;
#3675=ADVANCED_BREP_SHAPE_REPRESENTATION ( '', ( #9134, #12739 ), #6306 ) ;
#3689=ORIENTED_EDGE ( 'NONE', *, *, #19139, .T. ) ;
#3707=ADVANCED_FACE ( 'NONE', ( #16105 ), #3389, .T. ) ;
#3721=DIRECTION ( 'NONE',  ( -3.210834492181045054E-17, 2.441916418604790135E-15, 1.000000000000000000 ) ) ;
#3736=CIRCLE ( 'NONE', #12798, 6.000000000001509015 ) ;
#3826=AXIS2_PLACEMENT_3D ( 'NONE', #20506, #9836, #13506 ) ;
#3850=EDGE_CURVE ( 'NONE', #11752, #23191, #1213, .T. ) ;
#3851=CARTESIAN_POINT ( 'NONE',  ( -29.01760921662840076, 6.974057232812999274, -2.500000000000000000 ) ) ;
#3853=ADVANCED_FACE ( 'NONE', ( #23451 ), #18124, .T. ) ;
#3875=AXIS2_PLACEMENT_3D ( 'NONE', #4403, #9653, #470 ) ;
#3951=FACE_BOUND ( 'NONE', #16971, .T. ) ;
#3973=DIRECTION ( 'NONE',  ( 0.005235964011423952132, -0.9999862922464843873, 2.442051063554900023E-15 ) ) ;
#3975=CARTESIAN_POINT ( 'NONE',  ( -25.64168762722610140, 6.365828311191160438, -5.000000000000000000 ) ) ;
#3993=EDGE_CURVE ( 'NONE', #1846, #3168, #6110, .T. ) ;
#4063=VECTOR ( 'NONE', #11196, 999.9999999999998863 ) ;
#4216=VERTEX_POINT ( 'NONE', #14058 ) ;
#4313=DIRECTION ( 'NONE',  ( 1.000000000000000000, 3.210834492181040124E-17, 1.751623080406019734E-47 ) ) ;
#4326=ORIENTED_EDGE ( 'NONE', *, *, #18959, .T. ) ;
#4403=CARTESIAN_POINT ( 'NONE',  ( -19.49999999982360066, -0.1021026942259749964, -2.500000000000000000 ) ) ;
#4505=FACE_OUTER_BOUND ( 'NONE', #13681, .T. ) ;
#4559=CARTESIAN_POINT ( 'NONE',  ( -21.99941224366415682, -0.1563100308134279803, -3.750000000000000000 ) ) ;
#4627=CYLINDRICAL_SURFACE ( 'NONE', #12653, 2.500000000000000000 ) ;
#4628=ORIENTED_EDGE ( 'NONE', *, *, #22895, .T. ) ;
#4671=AXIS2_PLACEMENT_3D ( 'NONE', #8182, #22418, #15408 ) ;
#4725=ORIENTED_EDGE ( 'NONE', *, *, #8798, .F. ) ;
#4741=CARTESIAN_POINT ( 'NONE',  ( -32.64682763696299617, 7.329162855357650663, -5.000000000000000000 ) ) ;
#4743=CARTESIAN_POINT ( 'NONE',  ( -32.65701080836369385, 9.273987487686079945, -5.000000000000000000 ) ) ;
#4778=ORIENTED_EDGE ( 'NONE', *, *, #1483, .F. ) ;
#4808=DIRECTION ( 'NONE',  ( -3.210834492181045054E-17, 2.441916418604790135E-15, 1.000000000000000000 ) ) ;
#4817=DIRECTION ( 'NONE',  ( -3.210834492181040124E-17, 2.441916418604790135E-15, 1.000000000000000000 ) ) ;
#4827=CARTESIAN_POINT ( 'NONE',  ( -25.49858938551139786, -0.2322002804899460093, -3.750000000000000000 ) ) ;
#4867=DIRECTION ( 'NONE',  ( -0.9080662505692100872, 0.4188265566761218417, -1.040834085574018826E-15 ) ) ;
#4938=DIRECTION ( 'NONE',  ( -0.9997648975362233292, -0.02168293463498010415, 0.000000000000000000 ) ) ;
#4973=ADVANCED_FACE ( 'NONE', ( #14965 ), #22437, .F. ) ;
#5027=AXIS2_PLACEMENT_3D ( 'NONE', #11962, #15957, #17752 ) ;
#5058=( NAMED_UNIT ( * ) SI_UNIT ( $, .STERADIAN. ) SOLID_ANGLE_UNIT ( ) );
#5094=EDGE_LOOP ( 'NONE', ( #1668, #15648, #3689, #15305 ) ) ;
#5105=ORIENTED_EDGE ( 'NONE', *, *, #9354, .T. ) ;
#5136=FACE_OUTER_BOUND ( 'NONE', #6989, .T. ) ;
#5255=CYLINDRICAL_SURFACE ( 'NONE', #235, 49.22658835543908395 ) ;
#5295=ORIENTED_EDGE ( 'NONE', *, *, #313, .F. ) ;
#5304=CARTESIAN_POINT ( 'NONE',  ( -31.64684134471649912, 7.334398819369059908, -3.750000000000000000 ) ) ;
#5311=EDGE_LOOP ( 'NONE', ( #8292, #1196 ) ) ;
#5384=DIRECTION ( 'NONE',  ( -3.210834492181040124E-17, 2.441916418604790135E-15, 1.000000000000000000 ) ) ;
#5409=CARTESIAN_POINT ( 'NONE',  ( -16.50082286259691955, 23.02797946379192950, -2.500000000000059952 ) ) ;
#5446=DIRECTION ( 'NONE',  ( -3.210834492181045054E-17, 2.441916418604795262E-15, 1.000000000000000000 ) ) ;
#5466=ORIENTED_EDGE ( 'NONE', *, *, #8985, .T. ) ;
#5543=DIRECTION ( 'NONE',  ( 3.210834492181049985E-17, -2.441916418604790135E-15, -1.000000000000000000 ) ) ;
#5662=ORIENTED_EDGE ( 'NONE', *, *, #10248, .F. ) ;
#5700=VECTOR ( 'NONE', #15355, 1000.000000000000000 ) ;
#5726=EDGE_CURVE ( 'NONE', #1846, #10921, #13248, .T. ) ;
#5736=DIRECTION ( 'NONE',  ( -0.9997648975362233292, -0.02168293463498010415, 0.000000000000000000 ) ) ;
#5740=CARTESIAN_POINT ( 'NONE',  ( -20.00019857044559757, 22.95165872133759777, -5.000000000000060396 ) ) ;
#5747=EDGE_CURVE ( 'NONE', #18882, #4216, #14188, .T. ) ;
#5758=EDGE_CURVE ( 'NONE', #8468, #4216, #15134, .T. ) ;
#5825=VERTEX_POINT ( 'NONE', #3144 ) ;
#5845=ORIENTED_EDGE ( 'NONE', *, *, #11742, .F. ) ;
#5858=ORIENTED_EDGE ( 'NONE', *, *, #7249, .F. ) ;
#5873=EDGE_CURVE ( 'NONE', #17258, #1544, #18211, .T. ) ;
#5915=EDGE_CURVE ( 'NONE', #12721, #5825, #19992, .T. ) ;
#5917=ORIENTED_EDGE ( 'NONE', *, *, #18591, .T. ) ;
#6071=EDGE_LOOP ( 'NONE', ( #19780, #15351, #4628, #7743 ) ) ;
#6077=FACE_BOUND ( 'NONE', #5311, .T. ) ;
#6110=LINE ( 'NONE', #4559, #6924 ) ;
#6174=DIRECTION ( 'NONE',  ( -7.840589463879458156E-32, 2.441916418604790135E-15, 1.000000000000000000 ) ) ;
#6213=VECTOR ( 'NONE', #18549, 1000.000000000000000 ) ;
#6245=EDGE_LOOP ( 'NONE', ( #20073, #9858 ) ) ;
#6257=ORIENTED_EDGE ( 'NONE', *, *, #5915, .T. ) ;
#6258=LINE ( 'NONE', #13501, #13951 ) ;
#6272=CARTESIAN_POINT ( 'NONE',  ( -32.65701080836369385, 9.273987487686079945, -3.750000000000000000 ) ) ;
#6292=ORIENTED_EDGE ( 'NONE', *, *, #13495, .T. ) ;
#6306=( GEOMETRIC_REPRESENTATION_CONTEXT ( 3 ) GLOBAL_UNCERTAINTY_ASSIGNED_CONTEXT ( ( #16296 ) ) GLOBAL_UNIT_ASSIGNED_CONTEXT ( ( #3501, #3264, #5058 ) ) REPRESENTATION_CONTEXT ( 'NONE', 'WORKASPACE' ) );
#6370=ORIENTED_EDGE ( 'NONE', *, *, #7221, .F. ) ;
#6430=CARTESIAN_POINT ( 'NONE',  ( -16.50082286259691955, 23.02797946379192950, -5.000000000000060396 ) ) ;
#6482=DIRECTION ( 'NONE',  ( -3.210834492181045054E-17, 2.441916418604790135E-15, 1.000000000000000000 ) ) ;
#6556=ORIENTED_EDGE ( 'NONE', *, *, #545, .F. ) ;
#6599=ORIENTED_EDGE ( 'NONE', *, *, #6600, .F. ) ;
#6600=EDGE_CURVE ( 'NONE', #668, #3168, #7677, .T. ) ;
#6604=CARTESIAN_POINT ( 'NONE',  ( -32.42721070416779838, 10.33414378941739997, -3.750000000000000000 ) ) ;
#6646=EDGE_CURVE ( 'NONE', #551, #16156, #7733, .T. ) ;
#6758=ADVANCED_FACE ( 'NONE', ( #10116 ), #10230, .T. ) ;
#6810=ADVANCED_FACE ( 'NONE', ( #13897 ), #11783, .F. ) ;
#6887=ORIENTED_EDGE ( 'NONE', *, *, #14065, .F. ) ;
#6924=VECTOR ( 'NONE', #15369, 1000.000000000000000 ) ;
#6964=EDGE_CURVE ( 'NONE', #17890, #11752, #18045, .T. ) ;
#6979=CARTESIAN_POINT ( 'NONE',  ( -27.39127619791450030, 6.327883175579949615, -2.500000000000000000 ) ) ;
#6989=EDGE_LOOP ( 'NONE', ( #3547, #8640, #5466, #19103 ) ) ;
#7012=VERTEX_POINT ( 'NONE', #10937 ) ;
#7098=ORIENTED_EDGE ( 'NONE', *, *, #6964, .F. ) ;
#7108=EDGE_CURVE ( 'NONE', #10921, #1846, #15271, .T. ) ;
#7142=AXIS2_PLACEMENT_3D ( 'NONE', #18958, #6482, #15858 ) ;
#7155=ORIENTED_EDGE ( 'NONE', *, *, #22538, .T. ) ;
#7207=ORIENTED_EDGE ( 'NONE', *, *, #5915, .F. ) ;
#7221=EDGE_CURVE ( 'NONE', #7012, #8111, #22862, .T. ) ;
#7249=EDGE_CURVE ( 'NONE', #7455, #9721, #17654, .T. ) ;
#7258=ORIENTED_EDGE ( 'NONE', *, *, #19877, .F. ) ;
#7295=DIRECTION ( 'NONE',  ( 3.210834492181045054E-17, -2.441916418604790135E-15, -1.000000000000000000 ) ) ;
#7313=VECTOR ( 'NONE', #16366, 1000.000000000000114 ) ;
#7314=CARTESIAN_POINT ( 'NONE',  ( 34.24686308852899685, 12.59635270528730011, -5.000000000000000000 ) ) ;
#7321=AXIS2_PLACEMENT_3D ( 'NONE', #11456, #18807, #4313 ) ;
#7407=DIRECTION ( 'NONE',  ( -3.210834492181135034E-17, 2.441916418604790135E-15, 1.000000000000000000 ) ) ;
#7425=CARTESIAN_POINT ( 'NONE',  ( -20.00000000397369959, 22.95208919256949898, -2.500000000000059952 ) ) ;
#7428=DIRECTION ( 'NONE',  ( 3.210834492181139964E-17, -2.441916418604790135E-15, -1.000000000000000000 ) ) ;
#7433=CARTESIAN_POINT ( 'NONE',  ( -32.64682763696299617, 7.329162855357659545, -3.750000000000000000 ) ) ;
#7449=CIRCLE ( 'NONE', #17698, 3.499999999999999112 ) ;
#7455=VERTEX_POINT ( 'NONE', #21434 ) ;
#7464=CARTESIAN_POINT ( 'NONE',  ( -29.94694237017910154, 7.343299551231780242, -5.000000000000000000 ) ) ;
#7543=PLANE ( 'NONE',  #8279 ) ;
#7602=DIRECTION ( 'NONE',  ( -0.9997648975362233292, -0.02168293463497958373, 0.000000000000000000 ) ) ;
#7677=CIRCLE ( 'NONE', #3875, 2.500000000000000000 ) ;
#7721=EDGE_LOOP ( 'NONE', ( #12786, #17050 ) ) ;
#7733=LINE ( 'NONE', #20319, #6213 ) ;
#7743=ORIENTED_EDGE ( 'NONE', *, *, #6646, .F. ) ;
#7792=CARTESIAN_POINT ( 'NONE',  ( -17.00058775598304095, -0.04789535763852828532, -2.500000000000000000 ) ) ;
#7901=CARTESIAN_POINT ( 'NONE',  ( -32.42721070416779838, 10.33414378941739997, -5.000000000000000000 ) ) ;
#7915=DIRECTION ( 'NONE',  ( -0.9997648976141043642, -0.02168293104402130994, 0.000000000000000000 ) ) ;
#7926=DIRECTION ( 'NONE',  ( -0.9997648975362233292, -0.02168293463497999313, 0.000000000000000000 ) ) ;
#7927=ORIENTED_EDGE ( 'NONE', *, *, #19139, .F. ) ;
#7958=PLANE ( 'NONE',  #20030 ) ;
#8014=CARTESIAN_POINT ( 'NONE',  ( -30.15704507771850018, 9.287077397714901039, -5.000000000000000000 ) ) ;
#8033=DIRECTION ( 'NONE',  ( -3.210834492181040124E-17, 2.441916418604790135E-15, 1.000000000000000000 ) ) ;
#8053=ORIENTED_EDGE ( 'NONE', *, *, #5726, .F. ) ;
#8111=VERTEX_POINT ( 'NONE', #2600 ) ;
#8129=CARTESIAN_POINT ( 'NONE',  ( -23.49917714535047963, 22.87619892134707200, -3.750000000000059508 ) ) ;
#8172=ADVANCED_FACE ( 'NONE', ( #2484 ), #922, .T. ) ;
#8177=AXIS2_PLACEMENT_3D ( 'NONE', #5304, #12567, #21919 ) ;
#8182=CARTESIAN_POINT ( 'NONE',  ( -20.00019857044559757, 22.95165872133759777, -3.750000000000059508 ) ) ;
#8279=AXIS2_PLACEMENT_3D ( 'NONE', #20254, #3973, #16795 ) ;
#8292=ORIENTED_EDGE ( 'NONE', *, *, #12034, .T. ) ;
#8293=CARTESIAN_POINT ( 'NONE',  ( -23.49917714535047963, 22.87619892134707200, -2.500000000000059952 ) ) ;
#8306=CLOSED_SHELL ( 'NONE', ( #3570, #4973, #6810, #16778, #16191, #3707, #20742, #17439, #14046, #23340, #3853, #6758, #21050, #8172, #2897, #23461, #11715 ) ) ;
#8351=AXIS2_PLACEMENT_3D ( 'NONE', #699, #11315, #7602 ) ;
#8380=LINE ( 'NONE', #21188, #3404 ) ;
#8468=VERTEX_POINT ( 'NONE', #14685 ) ;
#8489=DIRECTION ( 'NONE',  ( 0.005235964011411631258, -0.9999862922464843873, 2.602085213965210642E-15 ) ) ;
#8519=CARTESIAN_POINT ( 'NONE',  ( -31.64684134471649912, 7.334398819369059908, -2.500000000000000000 ) ) ;
#8534=ORIENTED_EDGE ( 'NONE', *, *, #5758, .T. ) ;
#8640=ORIENTED_EDGE ( 'NONE', *, *, #17978, .F. ) ;
#8676=DIRECTION ( 'NONE',  ( -3.210834492180730126E-17, 2.441916418604790135E-15, 1.000000000000000000 ) ) ;
#8734=DIRECTION ( 'NONE',  ( 3.210834492181045054E-17, -2.441916418604790135E-15, -1.000000000000000000 ) ) ;
#8776=CARTESIAN_POINT ( 'NONE',  ( -25.44839750738890061, 25.46504853262640111, -3.750000000000069722 ) ) ;
#8798=EDGE_CURVE ( 'NONE', #1544, #2378, #10033, .T. ) ;
#8830=PRODUCT_DEFINITION_FORMATION_WITH_SPECIFIED_SOURCE ( 'ANY', '', #13107, .NOT_KNOWN. ) ;
#8985=EDGE_CURVE ( 'NONE', #9873, #18882, #1829, .T. ) ;
#9023=CIRCLE ( 'NONE', #16221, 49.22658835543908395 ) ;
#9064=EDGE_LOOP ( 'NONE', ( #5917, #20034, #12212, #12781 ) ) ;
#9070=FACE_OUTER_BOUND ( 'NONE', #5094, .T. ) ;
#9113=ORIENTED_EDGE ( 'NONE', *, *, #13495, .F. ) ;
#9134=MANIFOLD_SOLID_BREP ( 'Imported1', #8306 ) ;
#9218=DIRECTION ( 'NONE',  ( -0.9999862922464843873, -0.005235964011423952132, -1.932211830181250652E-17 ) ) ;
#9354=EDGE_CURVE ( 'NONE', #2378, #9721, #23131, .T. ) ;
#9395=VECTOR ( 'NONE', #21441, 1000.000000000000114 ) ;
#9449=ORIENTED_EDGE ( 'NONE', *, *, #13917, .F. ) ;
#9450=CARTESIAN_POINT ( 'NONE',  ( -31.64160538070510142, 6.334412527122579739, -2.500000000000000000 ) ) ;
#9607=CARTESIAN_POINT ( 'NONE',  ( -19.49999999982360066, -0.1021026942259779940, -3.750000000000000000 ) ) ;
#9642=AXIS2_PLACEMENT_3D ( 'NONE', #7464, #5446, #14697 ) ;
#9653=DIRECTION ( 'NONE',  ( 3.210834492181045054E-17, -2.441916418604790135E-15, -1.000000000000000000 ) ) ;
#9657=DIRECTION ( 'NONE',  ( -3.210834492181045054E-17, 2.441916418604790135E-15, 1.000000000000000000 ) ) ;
#9721=VERTEX_POINT ( 'NONE', #13099 ) ;
#9735=DIRECTION ( 'NONE',  ( -3.210834492181040124E-17, 2.441916418604790135E-15, 1.000000000000000000 ) ) ;
#9768=CARTESIAN_POINT ( 'NONE',  ( -21.99941224366415682, -0.1563100308134309779, -5.000000000000000000 ) ) ;
#9805=DIRECTION ( 'NONE',  ( -0.9080662505692100872, 0.4188265566761218417, -1.040834085574018826E-15 ) ) ;
#9836=DIRECTION ( 'NONE',  ( -3.210834492181049985E-17, 2.441916418604790135E-15, 1.000000000000000000 ) ) ;
#9858=ORIENTED_EDGE ( 'NONE', *, *, #6600, .T. ) ;
#9862=FACE_BOUND ( 'NONE', #6245, .T. ) ;
#9873=VERTEX_POINT ( 'NONE', #10023 ) ;
#9877=EDGE_CURVE ( 'NONE', #404, #17065, #1536, .T. ) ;
#9943=AXIS2_PLACEMENT_3D ( 'NONE', #13075, #11307, #14958 ) ;
#9952=ORIENTED_EDGE ( 'NONE', *, *, #13580, .T. ) ;
#10023=CARTESIAN_POINT ( 'NONE',  ( -25.44839750738890061, 25.46504853262630164, -5.000000000000070166 ) ) ;
#10033=CIRCLE ( 'NONE', #16060, 1.749999999999997780 ) ;
#10116=FACE_OUTER_BOUND ( 'NONE', #19725, .T. ) ;
#10171=DIRECTION ( 'NONE',  ( -3.210834492181045054E-17, 2.441916418604790135E-15, 1.000000000000000000 ) ) ;
#10230=CYLINDRICAL_SURFACE ( 'NONE', #13753, 2.500000000028980374 ) ;
#10245=AXIS2_PLACEMENT_3D ( 'NONE', #21426, #3367, #3016 ) ;
#10248=EDGE_CURVE ( 'NONE', #16249, #17065, #1128, .T. ) ;
#10351=EDGE_LOOP ( 'NONE', ( #604, #18842, #10580, #6257 ) ) ;
#10413=EDGE_LOOP ( 'NONE', ( #20313, #22566, #6556, #3558 ) ) ;
#10470=EDGE_LOOP ( 'NONE', ( #17233, #11201, #13813, #11397 ) ) ;
#10521=CARTESIAN_POINT ( 'NONE',  ( -19.49999999982360066, -0.1021026942259809916, -5.000000000000000000 ) ) ;
#10560=AXIS2_PLACEMENT_3D ( 'NONE', #10799, #18022, #1491 ) ;
#10580=ORIENTED_EDGE ( 'NONE', *, *, #3498, .T. ) ;
#10618=CARTESIAN_POINT ( 'NONE',  ( -25.64168762722610140, 6.365828311191170208, -2.500000000000000000 ) ) ;
#10799=CARTESIAN_POINT ( 'NONE',  ( -19.49999999982360066, -0.1021026942259749964, -2.500000000000000000 ) ) ;
#10921=VERTEX_POINT ( 'NONE', #14640 ) ;
#10923=AXIS2_PLACEMENT_3D ( 'NONE', #5740, #11115, #12995 ) ;
#10937=CARTESIAN_POINT ( 'NONE',  ( -31.64160538070510142, 6.334412527122579739, -2.500000000000000000 ) ) ;
#10967=LINE ( 'NONE', #11433, #21796 ) ;
#11115=DIRECTION ( 'NONE',  ( -3.210834492181180024E-17, 2.441916418604790135E-15, 1.000000000000000000 ) ) ;
#11196=DIRECTION ( 'NONE',  ( 0.9999862922464843873, 0.005235964011423952132, 1.932211830181250652E-17 ) ) ;
#11201=ORIENTED_EDGE ( 'NONE', *, *, #22125, .F. ) ;
#11224=PLANE ( 'NONE',  #7321 ) ;
#11254=LINE ( 'NONE', #9450, #11516 ) ;
#11307=DIRECTION ( 'NONE',  ( 3.210834492181180024E-17, -2.441916418604790135E-15, -1.000000000000000000 ) ) ;
#11315=DIRECTION ( 'NONE',  ( -3.210834492181045054E-17, 2.441916418604790135E-15, 1.000000000000000000 ) ) ;
#11397=ORIENTED_EDGE ( 'NONE', *, *, #20598, .T. ) ;
#11433=CARTESIAN_POINT ( 'NONE',  ( -32.65701080836369385, 9.273987487686079945, -2.500000000000000000 ) ) ;
#11456=CARTESIAN_POINT ( 'NONE',  ( -21.66397194015859640, 11.15562530387989959, -5.000000000000000000 ) ) ;
#11508=AXIS2_PLACEMENT_3D ( 'NONE', #18404, #13280, #2114 ) ;
#11516=VECTOR ( 'NONE', #9218, 999.9999999999998863 ) ;
#11538=AXIS2_PLACEMENT_3D ( 'NONE', #13928, #12392, #3348 ) ;
#11580=FACE_OUTER_BOUND ( 'NONE', #820, .T. ) ;
#11625=DIRECTION ( 'NONE',  ( -3.210834492181054915E-17, 2.441916418604790135E-15, 1.000000000000000000 ) ) ;
#11636=ORIENTED_EDGE ( 'NONE', *, *, #15055, .F. ) ;
#11715=ADVANCED_FACE ( 'NONE', ( #13077, #9862, #693 ), #7958, .T. ) ;
#11740=DIRECTION ( 'NONE',  ( -3.210834492181040124E-17, 2.441916418604790135E-15, 1.000000000000000000 ) ) ;
#11742=EDGE_CURVE ( 'NONE', #551, #1544, #1290, .T. ) ;
#11752=VERTEX_POINT ( 'NONE', #4741 ) ;
#11754=SHAPE_DEFINITION_REPRESENTATION ( #20690, #15060 ) ;
#11783=CYLINDRICAL_SURFACE ( 'NONE', #11894, 3.499999999999999112 ) ;
#11894=AXIS2_PLACEMENT_3D ( 'NONE', #21130, #17347, #1053 ) ;
#11962=CARTESIAN_POINT ( 'NONE',  ( 34.24686308852899685, 12.59635270528730011, -2.500000000000000000 ) ) ;
#11981=DIRECTION ( 'NONE',  ( -3.210834492181045054E-17, 2.441916418604790135E-15, 1.000000000000000000 ) ) ;
#12034=EDGE_CURVE ( 'NONE', #21214, #16249, #19644, .T. ) ;
#12076=EDGE_LOOP ( 'NONE', ( #5845, #13136, #19857, #16979, #9449, #1858, #5295, #6370, #22311, #225, #4725 ) ) ;
#12212=ORIENTED_EDGE ( 'NONE', *, *, #15055, .T. ) ;
#12293=ORIENTED_EDGE ( 'NONE', *, *, #12325, .F. ) ;
#12325=EDGE_CURVE ( 'NONE', #17065, #404, #13201, .T. ) ;
#12392=DIRECTION ( 'NONE',  ( -0.9080662505684728991, 0.4188265566777199522, -1.051895949684139634E-15 ) ) ;
#12535=DIRECTION ( 'NONE',  ( -0.9997648975362233292, -0.02168293463497958373, 0.000000000000000000 ) ) ;
#12567=DIRECTION ( 'NONE',  ( -3.210834492181045054E-17, 2.441916418604790135E-15, 1.000000000000000000 ) ) ;
#12645=AXIS2_PLACEMENT_3D ( 'NONE', #8519, #19424, #13961 ) ;
#12653=AXIS2_PLACEMENT_3D ( 'NONE', #19344, #21231, #20889 ) ;
#12721=VERTEX_POINT ( 'NONE', #19872 ) ;
#12739=AXIS2_PLACEMENT_3D ( 'NONE', #2569, #13380, #415 ) ;
#12755=CARTESIAN_POINT ( 'NONE',  ( -27.39127619791450030, 6.327883175579949615, -5.000000000000000000 ) ) ;
#12758=CYLINDRICAL_SURFACE ( 'NONE', #14910, 1.749999999999997780 ) ;
#12774=CARTESIAN_POINT ( 'NONE',  ( -29.01760921662840076, 6.974057232812999274, -5.000000000000000000 ) ) ;
#12778=DIRECTION ( 'NONE',  ( -0.005235964026270697493, 0.9999862922464064496, 1.340741286434373073E-35 ) ) ;
#12781=ORIENTED_EDGE ( 'NONE', *, *, #7249, .T. ) ;
#12786=ORIENTED_EDGE ( 'NONE', *, *, #9877, .T. ) ;
#12798=AXIS2_PLACEMENT_3D ( 'NONE', #14687, #5543, #20035 ) ;
#12879=DIRECTION ( 'NONE',  ( -0.4188265566777199522, -0.9080662505684728991, 2.203974058899820124E-15 ) ) ;
#12939=LINE ( 'NONE', #16970, #4063 ) ;
#12995=DIRECTION ( 'NONE',  ( 0.9822610636820822139, -0.1875185398144529336, 4.336808689942018229E-16 ) ) ;
#13075=CARTESIAN_POINT ( 'NONE',  ( -20.00019857044559757, 22.95165872133759777, -2.500000000000059952 ) ) ;
#13077=FACE_BOUND ( 'NONE', #7721, .T. ) ;
#13099=CARTESIAN_POINT ( 'NONE',  ( -29.94170640616770029, 6.343313258985349812, -2.500000000000000000 ) ) ;
#13107=PRODUCT ( '1602p_c_11', '1602p_c_11', '', ( #14596 ) ) ;
#13136=ORIENTED_EDGE ( 'NONE', *, *, #13332, .F. ) ;
#13201=CIRCLE ( 'NONE', #20020, 3.499999999999999112 ) ;
#13248=CIRCLE ( 'NONE', #3001, 2.500000000000000000 ) ;
#13262=VECTOR ( 'NONE', #5384, 1000.000000000000000 ) ;
#13276=LINE ( 'NONE', #6272, #2744 ) ;
#13280=DIRECTION ( 'NONE',  ( -3.210834492181045054E-17, 2.441916418604790135E-15, 1.000000000000000000 ) ) ;
#13332=EDGE_CURVE ( 'NONE', #5825, #551, #3736, .T. ) ;
#13380=DIRECTION ( 'NONE',  ( 0.000000000000000000, 0.000000000000000000, 1.000000000000000000 ) ) ;
#13426=DIRECTION ( 'NONE',  ( 1.000000000000000000, 3.210834492181040124E-17, 1.751623080406019734E-47 ) ) ;
#13444=DIRECTION ( 'NONE',  ( -0.9997648975362233292, -0.02168293463497958373, 0.000000000000000000 ) ) ;
#13495=EDGE_CURVE ( 'NONE', #21501, #638, #22622, .T. ) ;
#13501=CARTESIAN_POINT ( 'NONE',  ( -29.01760921662840076, 6.974057232812999274, -3.750000000000000000 ) ) ;
#13506=DIRECTION ( 'NONE',  ( -0.9997648976141043642, -0.02168293104402130300, 0.000000000000000000 ) ) ;
#13537=EDGE_LOOP ( 'NONE', ( #21843, #7258, #17205, #14000 ) ) ;
#13580=EDGE_CURVE ( 'NONE', #2399, #2378, #6258, .T. ) ;
#13681=EDGE_LOOP ( 'NONE', ( #16537, #8053, #21951, #6599 ) ) ;
#13744=AXIS2_PLACEMENT_3D ( 'NONE', #7433, #21790, #12778 ) ;
#13753=AXIS2_PLACEMENT_3D ( 'NONE', #2739, #8676, #4867 ) ;
#13813=ORIENTED_EDGE ( 'NONE', *, *, #3850, .T. ) ;
#13856=EDGE_CURVE ( 'NONE', #12721, #21501, #9023, .T. ) ;
#13897=FACE_OUTER_BOUND ( 'NONE', #14846, .T. ) ;
#13913=DIRECTION ( 'NONE',  ( 0.005235964011411631258, -0.9999862922464843873, 2.602085213965210642E-15 ) ) ;
#13917=EDGE_CURVE ( 'NONE', #4216, #16805, #16547, .T. ) ;
#13928=CARTESIAN_POINT ( 'NONE',  ( -25.44879460632040136, 25.46418757447539960, -3.750000000000069722 ) ) ;
#13945=ORIENTED_EDGE ( 'NONE', *, *, #17978, .T. ) ;
#13950=CARTESIAN_POINT ( 'NONE',  ( -31.64160538070510142, 6.334412527122569969, -3.750000000000000000 ) ) ;
#13951=VECTOR ( 'NONE', #11740, 1000.000000000000000 ) ;
#13961=DIRECTION ( 'NONE',  ( -0.9999862922464843873, -0.005235964011397749134, 0.000000000000000000 ) ) ;
#14000=ORIENTED_EDGE ( 'NONE', *, *, #22125, .T. ) ;
#14027=CYLINDRICAL_SURFACE ( 'NONE', #14555, 1.000000000000000000 ) ;
#14046=ADVANCED_FACE ( 'NONE', ( #15122 ), #7543, .T. ) ;
#14058=CARTESIAN_POINT ( 'NONE',  ( -32.42721070416779838, 10.33414378941739997, -2.500000000000000000 ) ) ;
#14063=AXIS2_PLACEMENT_3D ( 'NONE', #3097, #17251, #19150 ) ;
#14065=EDGE_CURVE ( 'NONE', #18882, #17890, #20780, .T. ) ;
#14084=ORIENTED_EDGE ( 'NONE', *, *, #3850, .F. ) ;
#14188=LINE ( 'NONE', #6604, #19705 ) ;
#14191=DIRECTION ( 'NONE',  ( -3.210834492181040124E-17, 2.441916418604790135E-15, 1.000000000000000000 ) ) ;
#14225=FACE_OUTER_BOUND ( 'NONE', #10470, .T. ) ;
#14373=FACE_OUTER_BOUND ( 'NONE', #1052, .T. ) ;
#14506=AXIS2_PLACEMENT_3D ( 'NONE', #3515, #16444, #16217 ) ;
#14540=AXIS2_PLACEMENT_3D ( 'NONE', #12755, #7295, #16299 ) ;
#14555=AXIS2_PLACEMENT_3D ( 'NONE', #16043, #1663, #13913 ) ;
#14596=MECHANICAL_CONTEXT ( 'NONE', #473, 'mechanical' ) ;
#14640=CARTESIAN_POINT ( 'NONE',  ( -17.00058775598304095, -0.04789535763852829919, -5.000000000000000000 ) ) ;
#14675=VECTOR ( 'NONE', #8033, 1000.000000000000000 ) ;
#14685=CARTESIAN_POINT ( 'NONE',  ( -32.65701080836369385, 9.273987487686079945, -2.500000000000000000 ) ) ;
#14687=CARTESIAN_POINT ( 'NONE',  ( -19.49999999982519938, -0.1021026942257829973, -2.500000000000000000 ) ) ;
#14697=DIRECTION ( 'NONE',  ( 0.005235964011411635595, -0.9999862922464843873, 2.602085213965213008E-15 ) ) ;
#14846=EDGE_LOOP ( 'NONE', ( #5662, #18728, #18170, #12293 ) ) ;
#14910=AXIS2_PLACEMENT_3D ( 'NONE', #18102, #3721, #5736 ) ;
#14958=DIRECTION ( 'NONE',  ( 0.9822610636820822139, -0.1875185398144529336, 5.059610138265687687E-16 ) ) ;
#14965=FACE_OUTER_BOUND ( 'NONE', #21819, .T. ) ;
#14979=VECTOR ( 'NONE', #205, 1000.000000000000114 ) ;
#15055=EDGE_CURVE ( 'NONE', #23191, #7455, #12939, .T. ) ;
#15060=SHAPE_REPRESENTATION ( '1602p_c_11', ( #12739 ), #6306 ) ;
#15122=FACE_OUTER_BOUND ( 'NONE', #9064, .T. ) ;
#15134=CIRCLE ( 'NONE', #10245, 2.500000000028980374 ) ;
#15142=FACE_OUTER_BOUND ( 'NONE', #10351, .T. ) ;
#15162=EDGE_CURVE ( 'NONE', #16805, #638, #17501, .T. ) ;
#15232=ORIENTED_EDGE ( 'NONE', *, *, #10248, .T. ) ;
#15254=ORIENTED_EDGE ( 'NONE', *, *, #14065, .T. ) ;
#15271=CIRCLE ( 'NONE', #11508, 2.500000000000000000 ) ;
#15305=ORIENTED_EDGE ( 'NONE', *, *, #5873, .T. ) ;
#15351=ORIENTED_EDGE ( 'NONE', *, *, #5873, .F. ) ;
#15355=DIRECTION ( 'NONE',  ( -3.210834492181045054E-17, 2.441916418604790135E-15, 1.000000000000000000 ) ) ;
#15369=DIRECTION ( 'NONE',  ( -3.210834492181045054E-17, 2.441916418604790135E-15, 1.000000000000000000 ) ) ;
#15403=ORIENTED_EDGE ( 'NONE', *, *, #5747, .F. ) ;
#15408=DIRECTION ( 'NONE',  ( 0.9822610636820822139, -0.1875185398144529336, 5.059610138265687687E-16 ) ) ;
#15597=CARTESIAN_POINT ( 'NONE',  ( -29.94694237017910154, 7.343299551231789124, -2.500000000000000000 ) ) ;
#15648=ORIENTED_EDGE ( 'NONE', *, *, #13580, .F. ) ;
#15658=VECTOR ( 'NONE', #14191, 1000.000000000000000 ) ;
#15707=VECTOR ( 'NONE', #12879, 1000.000000000000114 ) ;
#15756=DIRECTION ( 'NONE',  ( -0.02168293104353429326, 0.9997648976141146893, -5.786235142515748320E-35 ) ) ;
#15761=ORIENTED_EDGE ( 'NONE', *, *, #8985, .F. ) ;
#15785=DIRECTION ( 'NONE',  ( -3.210834492181040124E-17, 2.441916418604790135E-15, 1.000000000000000000 ) ) ;
#15858=DIRECTION ( 'NONE',  ( -0.9997648975362233292, -0.02168293463497958373, 0.000000000000000000 ) ) ;
#15957=DIRECTION ( 'NONE',  ( -3.210834492181139964E-17, 2.441916418604790135E-15, 1.000000000000000000 ) ) ;
#15967=SHAPE_REPRESENTATION_RELATIONSHIP ( 'NONE' , 'NONE' ,  #15060, #3675 ) ;
#15995=CARTESIAN_POINT ( 'NONE',  ( -25.49858938551139786, -0.2322002804899429840, -2.500000000000000000 ) ) ;
#16043=CARTESIAN_POINT ( 'NONE',  ( -29.94694237017910154, 7.343299551231789124, -3.750000000000000000 ) ) ;
#16060=AXIS2_PLACEMENT_3D ( 'NONE', #6979, #21322, #4938 ) ;
#16105=FACE_OUTER_BOUND ( 'NONE', #6071, .T. ) ;
#16114=CARTESIAN_POINT ( 'NONE',  ( -14.10663218835320087, 21.82654748245090204, -2.500000000000059952 ) ) ;
#16156=VERTEX_POINT ( 'NONE', #843 ) ;
#16191=ADVANCED_FACE ( 'NONE', ( #6077, #3951, #11580 ), #11224, .F. ) ;
#16217=DIRECTION ( 'NONE',  ( -0.9999862922464843873, -0.005235964011397749134, 0.000000000000000000 ) ) ;
#16221=AXIS2_PLACEMENT_3D ( 'NONE', #7314, #7428, #23327 ) ;
#16249=VERTEX_POINT ( 'NONE', #6430 ) ;
#16253=CARTESIAN_POINT ( 'NONE',  ( -32.65701080836369385, 9.273987487686079945, -5.000000000000000000 ) ) ;
#16285=VECTOR ( 'NONE', #375, 1000.000000000000000 ) ;
#16296=UNCERTAINTY_MEASURE_WITH_UNIT (LENGTH_MEASURE( 1.000000000000000082E-05 ), #3501, 'distance_accuracy_value', 'NONE');
#16299=DIRECTION ( 'NONE',  ( -0.9997648975362233292, -0.02168293463498010415, 0.000000000000000000 ) ) ;
#16366=DIRECTION ( 'NONE',  ( 0.005235964026270697493, -0.9999862922464064496, 2.442051063555178886E-15 ) ) ;
#16423=CARTESIAN_POINT ( 'NONE',  ( -25.64168762722610140, 6.365828311191170208, -3.750000000000000000 ) ) ;
#16444=DIRECTION ( 'NONE',  ( -3.210834492181045054E-17, 2.441916418604790135E-15, 1.000000000000000000 ) ) ;
#16488=CARTESIAN_POINT ( 'NONE',  ( -25.64168762722610140, 6.365828311191160438, -5.000000000000000000 ) ) ;
#16537=ORIENTED_EDGE ( 'NONE', *, *, #945, .F. ) ;
#16547=LINE ( 'NONE', #3380, #9395 ) ;
#16682=CYLINDRICAL_SURFACE ( 'NONE', #2492, 6.000000000001509015 ) ;
#16689=CARTESIAN_POINT ( 'NONE',  ( -14.10663218835320087, 21.82654748245090204, -3.750000000000059508 ) ) ;
#16778=ADVANCED_FACE ( 'NONE', ( #4505 ), #4627, .F. ) ;
#16795=DIRECTION ( 'NONE',  ( 0.000000000000000000, -2.442084539047825566E-15, -1.000000000000000000 ) ) ;
#16805=VERTEX_POINT ( 'NONE', #17231 ) ;
#16833=ORIENTED_EDGE ( 'NONE', *, *, #22895, .F. ) ;
#16970=CARTESIAN_POINT ( 'NONE',  ( -31.64160538070510142, 6.334412527122569969, -5.000000000000000000 ) ) ;
#16971=EDGE_LOOP ( 'NONE', ( #18532, #22158 ) ) ;
#16979=ORIENTED_EDGE ( 'NONE', *, *, #15162, .F. ) ;
#17050=ORIENTED_EDGE ( 'NONE', *, *, #12325, .T. ) ;
#17065=VERTEX_POINT ( 'NONE', #5409 ) ;
#17205=ORIENTED_EDGE ( 'NONE', *, *, #6964, .T. ) ;
#17231=CARTESIAN_POINT ( 'NONE',  ( -25.44839750738890061, 25.46504853262640111, -2.500000000000059952 ) ) ;
#17233=ORIENTED_EDGE ( 'NONE', *, *, #7221, .T. ) ;
#17251=DIRECTION ( 'NONE',  ( 3.210834492181045054E-17, -2.441916418604790135E-15, -1.000000000000000000 ) ) ;
#17258=VERTEX_POINT ( 'NONE', #3975 ) ;
#17347=DIRECTION ( 'NONE',  ( -3.210834492181045054E-17, 2.441916418604790135E-15, 1.000000000000000000 ) ) ;
#17439=ADVANCED_FACE ( 'NONE', ( #14373 ), #14027, .T. ) ;
#17501=CIRCLE ( 'NONE', #9943, 5.999999999999999112 ) ;
#17654=LINE ( 'NONE', #21081, #22112 ) ;
#17698=AXIS2_PLACEMENT_3D ( 'NONE', #18796, #9657, #13444 ) ;
#17752=DIRECTION ( 'NONE',  ( 0.9822637906114334294, -0.1875042550281410536, 4.933538860811975815E-16 ) ) ;
#17758=EDGE_LOOP ( 'NONE', ( #4326, #7207, #21397, #6292 ) ) ;
#17890=VERTEX_POINT ( 'NONE', #4743 ) ;
#17978=EDGE_CURVE ( 'NONE', #9873, #16805, #19343, .T. ) ;
#18022=DIRECTION ( 'NONE',  ( 3.210834492181045054E-17, -2.441916418604790135E-15, -1.000000000000000000 ) ) ;
#18045=LINE ( 'NONE', #16253, #7313 ) ;
#18095=PRODUCT_DEFINITION ( 'UNKNOWN', '', #8830, #18234 ) ;
#18102=CARTESIAN_POINT ( 'NONE',  ( -27.39127619791450030, 6.327883175579949615, -3.750000000000000000 ) ) ;
#18124=PLANE ( 'NONE',  #13744 ) ;
#18170=ORIENTED_EDGE ( 'NONE', *, *, #1483, .T. ) ;
#18200=EDGE_CURVE ( 'NONE', #7455, #2399, #18751, .T. ) ;
#18211=LINE ( 'NONE', #16423, #13262 ) ;
#18234=DESIGN_CONTEXT ( 'detailed design', #328, 'design' ) ;
#18314=CARTESIAN_POINT ( 'NONE',  ( -23.49917714535047963, 22.87619892134707200, -5.000000000000060396 ) ) ;
#18404=CARTESIAN_POINT ( 'NONE',  ( -19.49999999982360066, -0.1021026942259809916, -5.000000000000000000 ) ) ;
#18532=ORIENTED_EDGE ( 'NONE', *, *, #5726, .T. ) ;
#18549=DIRECTION ( 'NONE',  ( 3.210834492181040124E-17, -2.441916418604790135E-15, -1.000000000000000000 ) ) ;
#18591=EDGE_CURVE ( 'NONE', #9721, #7012, #11254, .T. ) ;
#18640=VECTOR ( 'NONE', #11981, 1000.000000000000000 ) ;
#18700=ORIENTED_EDGE ( 'NONE', *, *, #15162, .T. ) ;
#18728=ORIENTED_EDGE ( 'NONE', *, *, #12034, .F. ) ;
#18751=CIRCLE ( 'NONE', #9642, 0.9999999999999991118 ) ;
#18796=CARTESIAN_POINT ( 'NONE',  ( -20.00000000397369959, 22.95208919256949898, -5.000000000000060396 ) ) ;
#18807=DIRECTION ( 'NONE',  ( -7.840589463879458156E-32, 2.441916418604790135E-15, 1.000000000000000000 ) ) ;
#18842=ORIENTED_EDGE ( 'NONE', *, *, #6646, .T. ) ;
#18882=VERTEX_POINT ( 'NONE', #7901 ) ;
#18958=CARTESIAN_POINT ( 'NONE',  ( -20.00000000397369959, 22.95208919256949898, -5.000000000000060396 ) ) ;
#18959=EDGE_CURVE ( 'NONE', #638, #5825, #73, .T. ) ;
#18971=CYLINDRICAL_SURFACE ( 'NONE', #23165, 2.500000000000000000 ) ;
#19020=CIRCLE ( 'NONE', #3826, 6.000000000001509015 ) ;
#19103=ORIENTED_EDGE ( 'NONE', *, *, #5747, .T. ) ;
#19139=EDGE_CURVE ( 'NONE', #2399, #17258, #2398, .T. ) ;
#19142=EDGE_LOOP ( 'NONE', ( #18700, #9113, #7155, #13945 ) ) ;
#19150=DIRECTION ( 'NONE',  ( -0.9997648975362233292, -0.02168293463497958373, 0.000000000000000000 ) ) ;
#19343=LINE ( 'NONE', #8776, #19507 ) ;
#19344=CARTESIAN_POINT ( 'NONE',  ( -19.49999999982360066, -0.1021026942259779940, -3.750000000000000000 ) ) ;
#19424=DIRECTION ( 'NONE',  ( 3.210834492181045054E-17, -2.441916418604790135E-15, -1.000000000000000000 ) ) ;
#19498=ORIENTED_EDGE ( 'NONE', *, *, #1944, .F. ) ;
#19507=VECTOR ( 'NONE', #15785, 1000.000000000000000 ) ;
#19644=CIRCLE ( 'NONE', #7142, 3.499999999999999112 ) ;
#19662=CARTESIAN_POINT ( 'NONE',  ( -16.50082286259691955, 23.02797946379192950, -3.750000000000059508 ) ) ;
#19705=VECTOR ( 'NONE', #21071, 1000.000000000000000 ) ;
#19725=EDGE_LOOP ( 'NONE', ( #8534, #15403, #15254, #1549 ) ) ;
#19728=AXIS2_PLACEMENT_3D ( 'NONE', #15597, #22835, #8489 ) ;
#19780=ORIENTED_EDGE ( 'NONE', *, *, #11742, .T. ) ;
#19857=ORIENTED_EDGE ( 'NONE', *, *, #18959, .F. ) ;
#19858=ORIENTED_EDGE ( 'NONE', *, *, #3498, .F. ) ;
#19872=CARTESIAN_POINT ( 'NONE',  ( -13.66075527208050033, 1.277470069177119916, -5.000000000000000000 ) ) ;
#19877=EDGE_CURVE ( 'NONE', #17890, #8468, #13276, .T. ) ;
#19992=LINE ( 'NONE', #21877, #16285 ) ;
#20020=AXIS2_PLACEMENT_3D ( 'NONE', #7425, #8734, #12535 ) ;
#20030=AXIS2_PLACEMENT_3D ( 'NONE', #22431, #6174, #13426 ) ;
#20034=ORIENTED_EDGE ( 'NONE', *, *, #20598, .F. ) ;
#20035=DIRECTION ( 'NONE',  ( -0.9997648976141043642, -0.02168293104402130300, 0.000000000000000000 ) ) ;
#20073=ORIENTED_EDGE ( 'NONE', *, *, #545, .T. ) ;
#20254=CARTESIAN_POINT ( 'NONE',  ( -29.94170640616770029, 6.343313258985340042, -3.750000000000000000 ) ) ;
#20313=ORIENTED_EDGE ( 'NONE', *, *, #7108, .F. ) ;
#20319=CARTESIAN_POINT ( 'NONE',  ( -25.49858938551139786, -0.2322002804899460093, -3.750000000000000000 ) ) ;
#20501=DIRECTION ( 'NONE',  ( -3.210834492181040124E-17, 2.441916418604790135E-15, 1.000000000000000000 ) ) ;
#20506=CARTESIAN_POINT ( 'NONE',  ( -19.49999999982519938, -0.1021026942257889925, -5.000000000000000000 ) ) ;
#20598=EDGE_CURVE ( 'NONE', #23191, #7012, #23192, .T. ) ;
#20690=PRODUCT_DEFINITION_SHAPE ( 'NONE', 'NONE',  #18095 ) ;
#20742=ADVANCED_FACE ( 'NONE', ( #9070 ), #12758, .F. ) ;
#20780=CIRCLE ( 'NONE', #281, 2.500000000028980374 ) ;
#20886=ORIENTED_EDGE ( 'NONE', *, *, #9877, .F. ) ;
#20889=DIRECTION ( 'NONE',  ( -0.9997648975362233292, -0.02168293463497999313, 0.000000000000000000 ) ) ;
#20937=AXIS2_PLACEMENT_3D ( 'NONE', #4827, #23334, #15756 ) ;
#21016=CARTESIAN_POINT ( 'NONE',  ( -25.64168762722610140, 6.365828311191170208, -2.500000000000000000 ) ) ;
#21050=ADVANCED_FACE ( 'NONE', ( #5136 ), #3115, .T. ) ;
#21071=DIRECTION ( 'NONE',  ( -3.210834492181040124E-17, 2.441916418604790135E-15, 1.000000000000000000 ) ) ;
#21081=CARTESIAN_POINT ( 'NONE',  ( -29.94170640616770029, 6.343313258985340042, -3.750000000000000000 ) ) ;
#21130=CARTESIAN_POINT ( 'NONE',  ( -20.00000000397369959, 22.95208919256949898, -3.750000000000059508 ) ) ;
#21133=CIRCLE ( 'NONE', #10923, 5.999999999999999112 ) ;
#21188=CARTESIAN_POINT ( 'NONE',  ( -17.00058775598304095, -0.04789535763852829919, -3.750000000000000000 ) ) ;
#21214=VERTEX_POINT ( 'NONE', #18314 ) ;
#21231=DIRECTION ( 'NONE',  ( -3.210834492181045054E-17, 2.441916418604790135E-15, 1.000000000000000000 ) ) ;
#21322=DIRECTION ( 'NONE',  ( -3.210834492181045054E-17, 2.441916418604790135E-15, 1.000000000000000000 ) ) ;
#21384=ORIENTED_EDGE ( 'NONE', *, *, #13856, .F. ) ;
#21397=ORIENTED_EDGE ( 'NONE', *, *, #13856, .T. ) ;
#21426=CARTESIAN_POINT ( 'NONE',  ( -30.15704507771850018, 9.287077397714911697, -2.500000000000000000 ) ) ;
#21434=CARTESIAN_POINT ( 'NONE',  ( -29.94170640616770029, 6.343313258985340042, -5.000000000000000000 ) ) ;
#21441=DIRECTION ( 'NONE',  ( 0.4188265566777199522, 0.9080662505684728991, -2.203974058899820124E-15 ) ) ;
#21501=VERTEX_POINT ( 'NONE', #3650 ) ;
#21631=CARTESIAN_POINT ( 'NONE',  ( 34.24686308852899685, 12.59635270528730011, -3.750000000000000000 ) ) ;
#21790=DIRECTION ( 'NONE',  ( -0.9999862922464065607, -0.005235964026270698360, -1.932211826555549481E-17 ) ) ;
#21796=VECTOR ( 'NONE', #3183, 1000.000000000000114 ) ;
#21819=EDGE_LOOP ( 'NONE', ( #19498, #15232, #20886, #4778 ) ) ;
#21829=LINE ( 'NONE', #16488, #14979 ) ;
#21843=ORIENTED_EDGE ( 'NONE', *, *, #313, .T. ) ;
#21868=DIRECTION ( 'NONE',  ( 0.9822637906114334294, -0.1875042550281410536, 4.933538860811975815E-16 ) ) ;
#21877=CARTESIAN_POINT ( 'NONE',  ( -13.66075527208050033, 1.277470069177119916, -3.750000000000000000 ) ) ;
#21897=CARTESIAN_POINT ( 'NONE',  ( -25.44839750738890061, 25.46504853262630164, -5.000000000000070166 ) ) ;
#21919=DIRECTION ( 'NONE',  ( -0.9999862922464843873, -0.005235964011397749134, 0.000000000000000000 ) ) ;
#21951=ORIENTED_EDGE ( 'NONE', *, *, #3993, .T. ) ;
#22112=VECTOR ( 'NONE', #4817, 1000.000000000000000 ) ;
#22125=EDGE_CURVE ( 'NONE', #11752, #8111, #891, .T. ) ;
#22158=ORIENTED_EDGE ( 'NONE', *, *, #7108, .T. ) ;
#22242=DIRECTION ( 'NONE',  ( -3.210834492180725196E-17, 2.441916418604790135E-15, 1.000000000000000000 ) ) ;
#22273=VECTOR ( 'NONE', #20501, 1000.000000000000000 ) ;
#22311=ORIENTED_EDGE ( 'NONE', *, *, #18591, .F. ) ;
#22418=DIRECTION ( 'NONE',  ( -3.210834492181180024E-17, 2.441916418604790135E-15, 1.000000000000000000 ) ) ;
#22431=CARTESIAN_POINT ( 'NONE',  ( -21.66397194015859640, 11.15562530387989959, -2.500000000000000000 ) ) ;
#22437=CYLINDRICAL_SURFACE ( 'NONE', #8351, 3.499999999999999112 ) ;
#22538=EDGE_CURVE ( 'NONE', #21501, #9873, #21133, .T. ) ;
#22566=ORIENTED_EDGE ( 'NONE', *, *, #945, .T. ) ;
#22622=LINE ( 'NONE', #16689, #22273 ) ;
#22835=DIRECTION ( 'NONE',  ( 3.210834492181045054E-17, -2.441916418604795262E-15, -1.000000000000000000 ) ) ;
#22862=CIRCLE ( 'NONE', #12645, 1.000000000000000888 ) ;
#22895=EDGE_CURVE ( 'NONE', #17258, #16156, #21829, .T. ) ;
#23131=CIRCLE ( 'NONE', #19728, 1.000000000000000000 ) ;
#23165=AXIS2_PLACEMENT_3D ( 'NONE', #9607, #2692, #7926 ) ;
#23191=VERTEX_POINT ( 'NONE', #1278 ) ;
#23192=LINE ( 'NONE', #13950, #15658 ) ;
#23313=DIRECTION ( 'NONE',  ( -0.9997648975362233292, -0.02168293463498000007, 0.000000000000000000 ) ) ;
#23327=DIRECTION ( 'NONE',  ( 0.9822637906114334294, -0.1875042550281410536, 4.933538860811975815E-16 ) ) ;
#23334=DIRECTION ( 'NONE',  ( -0.9997648976141148003, -0.02168293104353429673, 2.084710914536959359E-17 ) ) ;
#23340=ADVANCED_FACE ( 'NONE', ( #14225 ), #3644, .T. ) ;
#23451=FACE_OUTER_BOUND ( 'NONE', #13537, .T. ) ;
#23461=ADVANCED_FACE ( 'NONE', ( #15142 ), #16682, .T. ) ;
#23550=COLOUR_RGB('Black', 0.08235294, 0.09019608, 0.10196078);
#23551=FILL_AREA_STYLE_COLOUR('',#23550);
#23552=FILL_AREA_STYLE('',(#23551));
#23553=SURFACE_STYLE_FILL_AREA(#23552);
#23554=SURFACE_SIDE_STYLE('',(#23553));
#23555=SURFACE_STYLE_USAGE(.BOTH.,#23554);
#23556=PRESENTATION_STYLE_ASSIGNMENT((#23555));
#23569=STYLED_ITEM('',(#23556),#9134);
#23570=MECHANICAL_DESIGN_GEOMETRIC_PRESENTATION_REPRESENTATION('',(#23569),#6306);
ENDSEC;
END-ISO-10303-21;
